ISO-10303-21;
HEADER;
/* Generated by software containing ST-Developer
 * from STEP Tools, Inc. (www.steptools.com) 
 */

FILE_DESCRIPTION(
/* description */ (''),
/* implementation_level */ '2;1');

FILE_NAME(
/* name */ 'M3_Screw_01 (1).step',
/* time_stamp */ '2026-10-22T15:07:41+06:00',
/* author */ (''),
/* organization */ (''),
/* preprocessor_version */ 'ST-DEVELOPER v20.2',
/* originating_system */ 'Autodesk Translation Framework v15.15.0.0',
/* authorisation */ '');

FILE_SCHEMA (('AUTOMOTIVE_DESIGN { 1 0 10303 214 3 1 1 }'));
ENDSEC;

DATA;
#10=MECHANICAL_DESIGN_GEOMETRIC_PRESENTATION_REPRESENTATION('',(#2881),#19220);
#70=SHAPE_REPRESENTATION_RELATIONSHIP('SRR','None',#19273,#84);
#84=ADVANCED_BREP_SHAPE_REPRESENTATION('',(#98),#19209);
#98=MANIFOLD_SOLID_BREP('M3_Screw_01',#11317);
#184=FACE_BOUND('',#3588,.T.);
#647=PLANE('',#11672);
#648=PLANE('',#11674);
#649=PLANE('',#11675);
#650=PLANE('',#11676);
#651=PLANE('',#11677);
#652=PLANE('',#11678);
#653=PLANE('',#11679);
#654=PLANE('',#11680);
#655=PLANE('',#11683);
#910=LINE('',#16456,#1765);
#911=LINE('',#16458,#1766);
#912=LINE('',#16460,#1767);
#913=LINE('',#16462,#1768);
#914=LINE('',#16464,#1769);
#915=LINE('',#16465,#1770);
#916=LINE('',#16470,#1771);
#917=LINE('',#16472,#1772);
#918=LINE('',#16473,#1773);
#919=LINE('',#16476,#1774);
#920=LINE('',#16477,#1775);
#921=LINE('',#16480,#1776);
#922=LINE('',#16481,#1777);
#923=LINE('',#16484,#1778);
#924=LINE('',#16485,#1779);
#925=LINE('',#16488,#1780);
#926=LINE('',#16489,#1781);
#927=LINE('',#16491,#1782);
#928=LINE('',#16496,#1783);
#1765=VECTOR('',#13179,10.);
#1766=VECTOR('',#13180,10.);
#1767=VECTOR('',#13181,10.);
#1768=VECTOR('',#13182,10.);
#1769=VECTOR('',#13183,10.);
#1770=VECTOR('',#13184,10.);
#1771=VECTOR('',#13189,10.);
#1772=VECTOR('',#13190,10.);
#1773=VECTOR('',#13191,10.);
#1774=VECTOR('',#13194,10.);
#1775=VECTOR('',#13195,10.);
#1776=VECTOR('',#13198,10.);
#1777=VECTOR('',#13199,10.);
#1778=VECTOR('',#13202,10.);
#1779=VECTOR('',#13203,10.);
#1780=VECTOR('',#13206,10.);
#1781=VECTOR('',#13207,10.);
#1782=VECTOR('',#13210,10.);
#1783=VECTOR('',#13217,1.49999999999999);
#2596=CYLINDRICAL_SURFACE('',#11681,1.4635);
#2881=STYLED_ITEM('',(#19410),#98);
#2966=FACE_OUTER_BOUND('',#3587,.T.);
#2967=FACE_OUTER_BOUND('',#3589,.T.);
#2968=FACE_OUTER_BOUND('',#3590,.T.);
#2969=FACE_OUTER_BOUND('',#3591,.T.);
#2970=FACE_OUTER_BOUND('',#3592,.T.);
#2971=FACE_OUTER_BOUND('',#3593,.T.);
#2972=FACE_OUTER_BOUND('',#3594,.T.);
#2973=FACE_OUTER_BOUND('',#3595,.T.);
#2974=FACE_OUTER_BOUND('',#3596,.T.);
#2975=FACE_OUTER_BOUND('',#3597,.T.);
#3587=EDGE_LOOP('',(#8074,#8075,#8076,#8077,#8078,#8079));
#3588=EDGE_LOOP('',(#8080));
#3589=EDGE_LOOP('',(#8081,#8082,#8083,#8084));
#3590=EDGE_LOOP('',(#8085,#8086,#8087,#8088));
#3591=EDGE_LOOP('',(#8089,#8090,#8091,#8092));
#3592=EDGE_LOOP('',(#8093,#8094,#8095,#8096));
#3593=EDGE_LOOP('',(#8097,#8098,#8099,#8100));
#3594=EDGE_LOOP('',(#8101,#8102,#8103,#8104));
#3595=EDGE_LOOP('',(#8105,#8106,#8107,#8108,#8109,#8110));
#3596=EDGE_LOOP('',(#8111,#8112,#8113,#8114));
#3597=EDGE_LOOP('',(#8115));
#4611=CIRCLE('',#11673,1.4635);
#4612=CIRCLE('',#11682,1.4635);
#5291=VERTEX_POINT('',#16454);
#5292=VERTEX_POINT('',#16455);
#5293=VERTEX_POINT('',#16457);
#5294=VERTEX_POINT('',#16459);
#5295=VERTEX_POINT('',#16461);
#5296=VERTEX_POINT('',#16463);
#5297=VERTEX_POINT('',#16466);
#5298=VERTEX_POINT('',#16469);
#5299=VERTEX_POINT('',#16471);
#5300=VERTEX_POINT('',#16475);
#5301=VERTEX_POINT('',#16479);
#5302=VERTEX_POINT('',#16483);
#5303=VERTEX_POINT('',#16487);
#5304=VERTEX_POINT('',#16494);
#6368=EDGE_CURVE('',#5291,#5292,#910,.T.);
#6369=EDGE_CURVE('',#5293,#5291,#911,.T.);
#6370=EDGE_CURVE('',#5294,#5293,#912,.T.);
#6371=EDGE_CURVE('',#5295,#5294,#913,.T.);
#6372=EDGE_CURVE('',#5296,#5295,#914,.T.);
#6373=EDGE_CURVE('',#5292,#5296,#915,.T.);
#6374=EDGE_CURVE('',#5297,#5297,#4611,.F.);
#6375=EDGE_CURVE('',#5291,#5298,#916,.T.);
#6376=EDGE_CURVE('',#5299,#5298,#917,.T.);
#6377=EDGE_CURVE('',#5293,#5299,#918,.T.);
#6378=EDGE_CURVE('',#5300,#5299,#919,.T.);
#6379=EDGE_CURVE('',#5294,#5300,#920,.T.);
#6380=EDGE_CURVE('',#5301,#5300,#921,.T.);
#6381=EDGE_CURVE('',#5295,#5301,#922,.T.);
#6382=EDGE_CURVE('',#5302,#5301,#923,.T.);
#6383=EDGE_CURVE('',#5296,#5302,#924,.T.);
#6384=EDGE_CURVE('',#5303,#5302,#925,.T.);
#6385=EDGE_CURVE('',#5292,#5303,#926,.T.);
#6386=EDGE_CURVE('',#5298,#5303,#927,.T.);
#6387=EDGE_CURVE('',#5304,#5304,#4612,.T.);
#6388=EDGE_CURVE('',#5304,#5297,#928,.T.);
#8074=ORIENTED_EDGE('',*,*,#6368,.F.);
#8075=ORIENTED_EDGE('',*,*,#6369,.F.);
#8076=ORIENTED_EDGE('',*,*,#6370,.F.);
#8077=ORIENTED_EDGE('',*,*,#6371,.F.);
#8078=ORIENTED_EDGE('',*,*,#6372,.F.);
#8079=ORIENTED_EDGE('',*,*,#6373,.F.);
#8080=ORIENTED_EDGE('',*,*,#6374,.T.);
#8081=ORIENTED_EDGE('',*,*,#6369,.T.);
#8082=ORIENTED_EDGE('',*,*,#6375,.T.);
#8083=ORIENTED_EDGE('',*,*,#6376,.F.);
#8084=ORIENTED_EDGE('',*,*,#6377,.F.);
#8085=ORIENTED_EDGE('',*,*,#6370,.T.);
#8086=ORIENTED_EDGE('',*,*,#6377,.T.);
#8087=ORIENTED_EDGE('',*,*,#6378,.F.);
#8088=ORIENTED_EDGE('',*,*,#6379,.F.);
#8089=ORIENTED_EDGE('',*,*,#6371,.T.);
#8090=ORIENTED_EDGE('',*,*,#6379,.T.);
#8091=ORIENTED_EDGE('',*,*,#6380,.F.);
#8092=ORIENTED_EDGE('',*,*,#6381,.F.);
#8093=ORIENTED_EDGE('',*,*,#6372,.T.);
#8094=ORIENTED_EDGE('',*,*,#6381,.T.);
#8095=ORIENTED_EDGE('',*,*,#6382,.F.);
#8096=ORIENTED_EDGE('',*,*,#6383,.F.);
#8097=ORIENTED_EDGE('',*,*,#6373,.T.);
#8098=ORIENTED_EDGE('',*,*,#6383,.T.);
#8099=ORIENTED_EDGE('',*,*,#6384,.F.);
#8100=ORIENTED_EDGE('',*,*,#6385,.F.);
#8101=ORIENTED_EDGE('',*,*,#6368,.T.);
#8102=ORIENTED_EDGE('',*,*,#6385,.T.);
#8103=ORIENTED_EDGE('',*,*,#6386,.F.);
#8104=ORIENTED_EDGE('',*,*,#6375,.F.);
#8105=ORIENTED_EDGE('',*,*,#6386,.T.);
#8106=ORIENTED_EDGE('',*,*,#6384,.T.);
#8107=ORIENTED_EDGE('',*,*,#6382,.T.);
#8108=ORIENTED_EDGE('',*,*,#6380,.T.);
#8109=ORIENTED_EDGE('',*,*,#6378,.T.);
#8110=ORIENTED_EDGE('',*,*,#6376,.T.);
#8111=ORIENTED_EDGE('',*,*,#6387,.F.);
#8112=ORIENTED_EDGE('',*,*,#6388,.T.);
#8113=ORIENTED_EDGE('',*,*,#6374,.F.);
#8114=ORIENTED_EDGE('',*,*,#6388,.F.);
#8115=ORIENTED_EDGE('',*,*,#6387,.T.);
#10842=ADVANCED_FACE('',(#2966,#184),#647,.F.);
#10843=ADVANCED_FACE('',(#2967),#648,.T.);
#10844=ADVANCED_FACE('',(#2968),#649,.T.);
#10845=ADVANCED_FACE('',(#2969),#650,.T.);
#10846=ADVANCED_FACE('',(#2970),#651,.T.);
#10847=ADVANCED_FACE('',(#2971),#652,.T.);
#10848=ADVANCED_FACE('',(#2972),#653,.T.);
#10849=ADVANCED_FACE('',(#2973),#654,.T.);
#10850=ADVANCED_FACE('',(#2974),#2596,.T.);
#10851=ADVANCED_FACE('',(#2975),#655,.F.);
#11317=CLOSED_SHELL('',(#10842,#10843,#10844,#10845,#10846,#10847,#10848,
#10849,#10850,#10851));
#11671=AXIS2_PLACEMENT_3D('',#16452,#13175,#13176);
#11672=AXIS2_PLACEMENT_3D('',#16453,#13177,#13178);
#11673=AXIS2_PLACEMENT_3D('',#16467,#13185,#13186);
#11674=AXIS2_PLACEMENT_3D('',#16468,#13187,#13188);
#11675=AXIS2_PLACEMENT_3D('',#16474,#13192,#13193);
#11676=AXIS2_PLACEMENT_3D('',#16478,#13196,#13197);
#11677=AXIS2_PLACEMENT_3D('',#16482,#13200,#13201);
#11678=AXIS2_PLACEMENT_3D('',#16486,#13204,#13205);
#11679=AXIS2_PLACEMENT_3D('',#16490,#13208,#13209);
#11680=AXIS2_PLACEMENT_3D('',#16492,#13211,#13212);
#11681=AXIS2_PLACEMENT_3D('',#16493,#13213,#13214);
#11682=AXIS2_PLACEMENT_3D('',#16495,#13215,#13216);
#11683=AXIS2_PLACEMENT_3D('',#16497,#13218,#13219);
#13175=DIRECTION('axis',(0.,0.,1.));
#13176=DIRECTION('refdir',(1.,0.,0.));
#13177=DIRECTION('center_axis',(0.,-1.,0.));
#13178=DIRECTION('ref_axis',(1.,0.,0.));
#13179=DIRECTION('',(0.427641188232285,0.,0.903948568297599));
#13180=DIRECTION('',(0.996663017976436,0.,0.0816261514350802));
#13181=DIRECTION('',(0.569021829744153,0.,-0.82232241686252));
#13182=DIRECTION('',(-0.427641188232283,0.,-0.9039485682976));
#13183=DIRECTION('',(-0.996663017976436,0.,-0.0816261514350783));
#13184=DIRECTION('',(-0.569021829744152,0.,0.822322416862521));
#13185=DIRECTION('center_axis',(0.,1.,0.));
#13186=DIRECTION('ref_axis',(1.,0.,0.));
#13187=DIRECTION('center_axis',(0.0816261514350802,0.,-0.996663017976436));
#13188=DIRECTION('ref_axis',(0.996663017976436,0.,0.0816261514350802));
#13189=DIRECTION('',(0.,-1.,0.));
#13190=DIRECTION('',(0.996663017976436,0.,0.0816261514350802));
#13191=DIRECTION('',(0.,-1.,0.));
#13192=DIRECTION('center_axis',(-0.82232241686252,0.,-0.569021829744153));
#13193=DIRECTION('ref_axis',(0.569021829744153,0.,-0.82232241686252));
#13194=DIRECTION('',(0.569021829744153,0.,-0.82232241686252));
#13195=DIRECTION('',(0.,-1.,0.));
#13196=DIRECTION('center_axis',(-0.9039485682976,0.,0.427641188232283));
#13197=DIRECTION('ref_axis',(-0.427641188232283,0.,-0.9039485682976));
#13198=DIRECTION('',(-0.427641188232283,0.,-0.9039485682976));
#13199=DIRECTION('',(0.,-1.,0.));
#13200=DIRECTION('center_axis',(-0.0816261514350783,0.,0.996663017976436));
#13201=DIRECTION('ref_axis',(-0.996663017976436,0.,-0.0816261514350783));
#13202=DIRECTION('',(-0.996663017976436,0.,-0.0816261514350783));
#13203=DIRECTION('',(0.,-1.,0.));
#13204=DIRECTION('center_axis',(0.822322416862521,0.,0.569021829744152));
#13205=DIRECTION('ref_axis',(-0.569021829744152,0.,0.822322416862521));
#13206=DIRECTION('',(-0.569021829744152,0.,0.822322416862521));
#13207=DIRECTION('',(0.,-1.,0.));
#13208=DIRECTION('center_axis',(0.903948568297599,0.,-0.427641188232285));
#13209=DIRECTION('ref_axis',(0.427641188232285,0.,0.903948568297599));
#13210=DIRECTION('',(0.427641188232285,0.,0.903948568297599));
#13211=DIRECTION('center_axis',(0.,-1.,0.));
#13212=DIRECTION('ref_axis',(1.,0.,0.));
#13213=DIRECTION('center_axis',(0.,1.,0.));
#13214=DIRECTION('ref_axis',(1.,0.,0.));
#13215=DIRECTION('center_axis',(0.,1.,0.));
#13216=DIRECTION('ref_axis',(1.,0.,0.));
#13217=DIRECTION('',(0.,-1.,0.));
#13218=DIRECTION('center_axis',(0.,-1.,0.));
#13219=DIRECTION('ref_axis',(1.,0.,0.));
#16452=CARTESIAN_POINT('',(0.,0.,0.));
#16453=CARTESIAN_POINT('Origin',(363.987734179926,50.,25.7372649179816));
#16454=CARTESIAN_POINT('',(365.301833806237,50.,23.8381926430366));
#16455=CARTESIAN_POINT('',(366.289428826807,50.,25.9257724399974));
#16456=CARTESIAN_POINT('',(365.301833806237,50.,23.8381926430366));
#16457=CARTESIAN_POINT('',(363.000139159357,50.,23.6496851210208));
#16458=CARTESIAN_POINT('',(363.000139159357,50.,23.6496851210208));
#16459=CARTESIAN_POINT('',(361.686039533046,50.,25.5487573959657));
#16460=CARTESIAN_POINT('',(361.686039533046,50.,25.5487573959657));
#16461=CARTESIAN_POINT('',(362.673634553616,50.,27.6363371929265));
#16462=CARTESIAN_POINT('',(362.673634553616,50.,27.6363371929265));
#16463=CARTESIAN_POINT('',(364.975329200496,50.,27.8248447149424));
#16464=CARTESIAN_POINT('',(364.975329200496,50.,27.8248447149424));
#16465=CARTESIAN_POINT('',(366.289428826807,50.,25.9257724399974));
#16466=CARTESIAN_POINT('',(362.524234179926,50.,25.7372649179816));
#16467=CARTESIAN_POINT('Origin',(363.987734179926,50.,25.7372649179816));
#16468=CARTESIAN_POINT('Origin',(363.000139159357,50.,23.6496851210208));
#16469=CARTESIAN_POINT('',(365.301833806237,49.,23.8381926430366));
#16470=CARTESIAN_POINT('',(365.301833806237,50.,23.8381926430366));
#16471=CARTESIAN_POINT('',(363.000139159357,49.,23.6496851210208));
#16472=CARTESIAN_POINT('',(363.000139159357,49.,23.6496851210208));
#16473=CARTESIAN_POINT('',(363.000139159357,50.,23.6496851210208));
#16474=CARTESIAN_POINT('Origin',(361.686039533046,50.,25.5487573959657));
#16475=CARTESIAN_POINT('',(361.686039533046,49.,25.5487573959657));
#16476=CARTESIAN_POINT('',(361.686039533046,49.,25.5487573959657));
#16477=CARTESIAN_POINT('',(361.686039533046,50.,25.5487573959657));
#16478=CARTESIAN_POINT('Origin',(362.673634553616,50.,27.6363371929265));
#16479=CARTESIAN_POINT('',(362.673634553616,49.,27.6363371929265));
#16480=CARTESIAN_POINT('',(362.673634553616,49.,27.6363371929265));
#16481=CARTESIAN_POINT('',(362.673634553616,50.,27.6363371929265));
#16482=CARTESIAN_POINT('Origin',(364.975329200496,50.,27.8248447149424));
#16483=CARTESIAN_POINT('',(364.975329200496,49.,27.8248447149424));
#16484=CARTESIAN_POINT('',(364.975329200496,49.,27.8248447149424));
#16485=CARTESIAN_POINT('',(364.975329200496,50.,27.8248447149424));
#16486=CARTESIAN_POINT('Origin',(366.289428826807,50.,25.9257724399974));
#16487=CARTESIAN_POINT('',(366.289428826807,49.,25.9257724399974));
#16488=CARTESIAN_POINT('',(366.289428826807,49.,25.9257724399974));
#16489=CARTESIAN_POINT('',(366.289428826807,50.,25.9257724399974));
#16490=CARTESIAN_POINT('Origin',(365.301833806237,50.,23.8381926430366));
#16491=CARTESIAN_POINT('',(365.301833806237,49.,23.8381926430366));
#16492=CARTESIAN_POINT('Origin',(363.987734179926,49.,25.7372649179816));
#16493=CARTESIAN_POINT('Origin',(363.987734179926,50.,25.7372649179816));
#16494=CARTESIAN_POINT('',(362.524234179926,63.,25.7372649179816));
#16495=CARTESIAN_POINT('Origin',(363.987734179926,63.,25.7372649179816));
#16496=CARTESIAN_POINT('',(362.524234179926,50.,25.7372649179816));
#16497=CARTESIAN_POINT('Origin',(363.987734179926,63.,25.7372649179816));
#19193=UNCERTAINTY_MEASURE_WITH_UNIT(LENGTH_MEASURE(0.01),#19221,
'DISTANCE_ACCURACY_VALUE',
'Maximum model space distance between geometric entities at asserted c
onnectivities');
#19204=UNCERTAINTY_MEASURE_WITH_UNIT(LENGTH_MEASURE(0.01),#19221,
'DISTANCE_ACCURACY_VALUE',
'Maximum model space distance between geometric entities at asserted c
onnectivities');
#19209=(
GEOMETRIC_REPRESENTATION_CONTEXT(3)
GLOBAL_UNCERTAINTY_ASSIGNED_CONTEXT((#19193))
GLOBAL_UNIT_ASSIGNED_CONTEXT((#19221,#19223,#19224))
REPRESENTATION_CONTEXT('','3D')
);
#19220=(
GEOMETRIC_REPRESENTATION_CONTEXT(3)
GLOBAL_UNCERTAINTY_ASSIGNED_CONTEXT((#19204))
GLOBAL_UNIT_ASSIGNED_CONTEXT((#19221,#19223,#19224))
REPRESENTATION_CONTEXT('','3D')
);
#19221=(
LENGTH_UNIT()
NAMED_UNIT(*)
SI_UNIT(.MILLI.,.METRE.)
);
#19223=(
NAMED_UNIT(*)
PLANE_ANGLE_UNIT()
SI_UNIT($,.RADIAN.)
);
#19224=(
NAMED_UNIT(*)
SI_UNIT($,.STERADIAN.)
SOLID_ANGLE_UNIT()
);
#19229=SHAPE_DEFINITION_REPRESENTATION(#19244,#19273);
#19244=PRODUCT_DEFINITION_SHAPE('',$,#19289);
#19273=SHAPE_REPRESENTATION('',(#11671),#19209);
#19284=PRODUCT_DEFINITION_CONTEXT('part definition',#19331,'design');
#19289=PRODUCT_DEFINITION('M3_Screw_01 (1)','M3_Screw_01 (1)',#19304,#19284);
#19304=PRODUCT_DEFINITION_FORMATION('',$,#19337);
#19331=APPLICATION_CONTEXT(
'Core Data for Automotive Mechanical Design Process');
#19332=PRODUCT_CONTEXT('part definition',#19331,'mechanical');
#19337=PRODUCT('M3_Screw_01 (1)','M3_Screw_01 (1)',$,(#19332));
#19404=COLOUR_RGB('Black',0.12,0.14,0.17);
#19405=FILL_AREA_STYLE_COLOUR('',#19404);
#19406=FILL_AREA_STYLE('',(#19405));
#19407=SURFACE_STYLE_FILL_AREA(#19406);
#19408=SURFACE_SIDE_STYLE('',(#19407));
#19409=SURFACE_STYLE_USAGE(.BOTH.,#19408);
#19410=PRESENTATION_STYLE_ASSIGNMENT((#19409));
ENDSEC;
END-ISO-10303-21;
